ISO-10303-21;
HEADER;
FILE_DESCRIPTION (('STEP AP214'),
    '1' );
FILE_NAME ('Battery.step',
    '2026-10-07T19:06:49',
    ( '' ),
    ( '' ),
    'SwSTEP 2.0',
    'SolidWorks 2020',
    '' );
FILE_SCHEMA (( 'AUTOMOTIVE_DESIGN' ));
ENDSEC;

DATA;
#69=CARTESIAN_POINT ( 'NONE',  ( -0.5999999999999999778, -5.000000000000000000, 0.5999999999999999778 ) ) ;
#91=ORIENTED_EDGE ( 'NONE', *, *, #55507, .T. ) ;
#105=AXIS2_PLACEMENT_3D ( 'NONE', #46882, #51305, #55725 ) ;
#127=DIRECTION ( 'NONE',  ( 0.000000000000000000, -1.000000000000000000, 0.000000000000000000 ) ) ;
#167=EDGE_CURVE ( 'NONE', #8218, #23965, #8695, .T. ) ;
#283=EDGE_LOOP ( 'NONE', ( #8504, #30368, #4564, #9836 ) ) ;
#361=CARTESIAN_POINT ( 'NONE',  ( -0.5999999999999999778, -5.200000000000000178, 0.5999999999999999778 ) ) ;
#433=CARTESIAN_POINT ( 'NONE',  ( -8.500000000000000000, -73.00000000000001421, 0.000000000000000000 ) ) ;
#574=ORIENTED_EDGE ( 'NONE', *, *, #53036, .T. ) ;
#670=VERTEX_POINT ( 'NONE', #3515 ) ;
#777=DIRECTION ( 'NONE',  ( 0.000000000000000000, 0.000000000000000000, 1.000000000000000000 ) ) ;
#807=DIRECTION ( 'NONE',  ( 0.000000000000000000, 1.000000000000000000, 0.000000000000000000 ) ) ;
#810=ADVANCED_FACE ( 'NONE', ( #55743 ), #50973, .T. ) ;
#969=PLANE ( 'NONE',  #18971 ) ;
#1062=DIRECTION ( 'NONE',  ( 0.000000000000000000, 0.000000000000000000, 1.000000000000000000 ) ) ;
#1124=VECTOR ( 'NONE', #51841, 1000.000000000000000 ) ;
#1127=DIRECTION ( 'NONE',  ( 0.000000000000000000, 0.000000000000000000, 1.000000000000000000 ) ) ;
#1255=VERTEX_POINT ( 'NONE', #57739 ) ;
#1413=LINE ( 'NONE', #40964, #10798 ) ;
#1456=ORIENTED_EDGE ( 'NONE', *, *, #46971, .F. ) ;
#1539=CARTESIAN_POINT ( 'NONE',  ( 0.000000000000000000, -74.80000000000001137, 0.000000000000000000 ) ) ;
#1986=CARTESIAN_POINT ( 'NONE',  ( -0.5999999999999999778, -5.200000000000000178, -4.000000000000000000 ) ) ;
#2048=VERTEX_POINT ( 'NONE', #45581 ) ;
#2106=DIRECTION ( 'NONE',  ( 0.000000000000000000, 0.000000000000000000, -1.000000000000000000 ) ) ;
#2128=CARTESIAN_POINT ( 'NONE',  ( -0.5999999999999999778, -5.000000000000000000, -0.5999999999999999778 ) ) ;
#2258=ORIENTED_EDGE ( 'NONE', *, *, #54684, .F. ) ;
#2267=CLOSED_SHELL ( 'NONE', ( #13427, #10694, #38626, #40692, #16760, #28341, #8235, #6042, #56094, #3598, #44706, #44437, #56570, #53806, #8409, #18427, #13506, #33732, #6776, #13616, #34124, #45071, #13215, #810, #51759, #14698 ) ) ;
#2554=CARTESIAN_POINT ( 'NONE',  ( -4.000000000000000000, -75.00000000000001421, 0.5999999999999999778 ) ) ;
#2598=VERTEX_POINT ( 'NONE', #46243 ) ;
#2853=FILL_AREA_STYLE ('',( #43298 ) ) ;
#2948=ORIENTED_EDGE ( 'NONE', *, *, #19155, .T. ) ;
#2950=VECTOR ( 'NONE', #33858, 1000.000000000000000 ) ;
#3121=( LENGTH_UNIT ( ) NAMED_UNIT ( * ) SI_UNIT ( .MILLI., .METRE. ) );
#3311=ORIENTED_EDGE ( 'NONE', *, *, #26106, .F. ) ;
#3357=CARTESIAN_POINT ( 'NONE',  ( -4.000000000000000000, -5.200000000000000178, 0.5999999999999999778 ) ) ;
#3403=( NAMED_UNIT ( * ) PLANE_ANGLE_UNIT ( ) SI_UNIT ( $, .RADIAN. ) );
#3484=CARTESIAN_POINT ( 'NONE',  ( 0.5999999999999999778, -5.000000000000000000, -0.5999999999999999778 ) ) ;
#3515=CARTESIAN_POINT ( 'NONE',  ( -0.5999999999999999778, -5.200000000000000178, 4.000000000000000000 ) ) ;
#3536=AXIS2_PLACEMENT_3D ( 'NONE', #38996, #20421, #38704 ) ;
#3598=ADVANCED_FACE ( 'NONE', ( #47845 ), #29790, .F. ) ;
#3962=ORIENTED_EDGE ( 'NONE', *, *, #50470, .T. ) ;
#4204=ORIENTED_EDGE ( 'NONE', *, *, #55099, .T. ) ;
#4219=FACE_BOUND ( 'NONE', #7187, .T. ) ;
#4374=LINE ( 'NONE', #40387, #52388 ) ;
#4385=CARTESIAN_POINT ( 'NONE',  ( 8.500000000000000000, -7.000000000000000000, 0.000000000000000000 ) ) ;
#4441=EDGE_CURVE ( 'NONE', #1255, #39893, #43523, .T. ) ;
#4564=ORIENTED_EDGE ( 'NONE', *, *, #31426, .F. ) ;
#4601=LINE ( 'NONE', #14310, #5260 ) ;
#4644=ORIENTED_EDGE ( 'NONE', *, *, #19378, .T. ) ;
#4669=PRODUCT_DEFINITION_FORMATION_WITH_SPECIFIED_SOURCE ( 'ANY', '', #40385, .NOT_KNOWN. ) ;
#4722=EDGE_CURVE ( 'NONE', #29661, #34312, #8215, .T. ) ;
#4730=LINE ( 'NONE', #54894, #36062 ) ;
#4796=DIRECTION ( 'NONE',  ( 0.000000000000000000, 0.000000000000000000, 1.000000000000000000 ) ) ;
#4819=FACE_OUTER_BOUND ( 'NONE', #23078, .T. ) ;
#4871=ORIENTED_EDGE ( 'NONE', *, *, #21468, .T. ) ;
#4993=VECTOR ( 'NONE', #49259, 1000.000000000000000 ) ;
#5038=AXIS2_PLACEMENT_3D ( 'NONE', #45735, #32697, #28268 ) ;
#5185=VECTOR ( 'NONE', #29673, 1000.000000000000000 ) ;
#5210=CARTESIAN_POINT ( 'NONE',  ( 0.5999999999999999778, -5.200000000000000178, -4.000000000000000000 ) ) ;
#5260=VECTOR ( 'NONE', #1062, 1000.000000000000000 ) ;
#5302=VECTOR ( 'NONE', #58176, 1000.000000000000000 ) ;
#5431=SHAPE_REPRESENTATION_RELATIONSHIP ( 'NONE' , 'NONE' ,  #13452, #35529 ) ;
#5585=CARTESIAN_POINT ( 'NONE',  ( 0.000000000000000000, -5.000000000000000000, 0.000000000000000000 ) ) ;
#5599=LINE ( 'NONE', #23610, #50349 ) ;
#5644=AXIS2_PLACEMENT_3D ( 'NONE', #10167, #46196, #5721 ) ;
#5715=ORIENTED_EDGE ( 'NONE', *, *, #167, .T. ) ;
#5721=DIRECTION ( 'NONE',  ( -0.9999380042107527400, 0.000000000000000000, 0.01113497799803945566 ) ) ;
#5792=CARTESIAN_POINT ( 'NONE',  ( -10.50000000000000000, -73.00000000000001421, 0.000000000000000000 ) ) ;
#5817=PLANE ( 'NONE',  #38665 ) ;
#5831=ORIENTED_EDGE ( 'NONE', *, *, #40673, .T. ) ;
#5949=PLANE ( 'NONE',  #24379 ) ;
#5976=EDGE_LOOP ( 'NONE', ( #20885, #35365, #38386, #29389 ) ) ;
#6001=ORIENTED_EDGE ( 'NONE', *, *, #26106, .T. ) ;
#6042=ADVANCED_FACE ( 'NONE', ( #25482 ), #47374, .F. ) ;
#6071=ORIENTED_EDGE ( 'NONE', *, *, #55507, .F. ) ;
#6088=ORIENTED_EDGE ( 'NONE', *, *, #38472, .F. ) ;
#6222=ORIENTED_EDGE ( 'NONE', *, *, #35877, .T. ) ;
#6307=DIRECTION ( 'NONE',  ( 1.000000000000000000, 0.000000000000000000, 0.000000000000000000 ) ) ;
#6383=ORIENTED_EDGE ( 'NONE', *, *, #12073, .F. ) ;
#6575=ORIENTED_EDGE ( 'NONE', *, *, #46924, .T. ) ;
#6632=CARTESIAN_POINT ( 'NONE',  ( 4.000000000000000000, -5.000000000000000000, 0.5999999999999999778 ) ) ;
#6737=ORIENTED_EDGE ( 'NONE', *, *, #39116, .F. ) ;
#6764=EDGE_CURVE ( 'NONE', #22013, #36179, #4730, .T. ) ;
#6776=ADVANCED_FACE ( 'NONE', ( #23887 ), #22729, .T. ) ;
#7187=EDGE_LOOP ( 'NONE', ( #10451, #45779, #14340, #24674 ) ) ;
#7376=DIRECTION ( 'NONE',  ( 0.000000000000000000, 0.000000000000000000, -1.000000000000000000 ) ) ;
#7515=VECTOR ( 'NONE', #10175, 1000.000000000000000 ) ;
#7580=ORIENTED_EDGE ( 'NONE', *, *, #53504, .T. ) ;
#7631=EDGE_CURVE ( 'NONE', #42169, #34312, #26285, .T. ) ;
#7753=ORIENTED_EDGE ( 'NONE', *, *, #45812, .T. ) ;
#7825=ORIENTED_EDGE ( 'NONE', *, *, #50998, .F. ) ;
#7882=AXIS2_PLACEMENT_3D ( 'NONE', #20372, #25650, #43676 ) ;
#7924=DIRECTION ( 'NONE',  ( -1.000000000000000000, 0.000000000000000000, 0.000000000000000000 ) ) ;
#8110=DIRECTION ( 'NONE',  ( 0.000000000000000000, 0.000000000000000000, 1.000000000000000000 ) ) ;
#8215=LINE ( 'NONE', #16219, #49524 ) ;
#8218=VERTEX_POINT ( 'NONE', #56806 ) ;
#8235=ADVANCED_FACE ( 'NONE', ( #20220 ), #30205, .F. ) ;
#8409=ADVANCED_FACE ( 'NONE', ( #4819 ), #34919, .F. ) ;
#8481=DIRECTION ( 'NONE',  ( 0.000000000000000000, 0.000000000000000000, 1.000000000000000000 ) ) ;
#8504=ORIENTED_EDGE ( 'NONE', *, *, #26955, .T. ) ;
#8612=ORIENTED_EDGE ( 'NONE', *, *, #41158, .T. ) ;
#8677=AXIS2_PLACEMENT_3D ( 'NONE', #25196, #57073, #57362 ) ;
#8695=LINE ( 'NONE', #49746, #54176 ) ;
#8996=LINE ( 'NONE', #27563, #50008 ) ;
#9038=EDGE_CURVE ( 'NONE', #46323, #21810, #41340, .T. ) ;
#9107=VECTOR ( 'NONE', #42067, 1000.000000000000000 ) ;
#9193=DIRECTION ( 'NONE',  ( -1.000000000000000000, 0.000000000000000000, 0.000000000000000000 ) ) ;
#9203=EDGE_LOOP ( 'NONE', ( #8612, #14726, #6071, #574 ) ) ;
#9351=DIRECTION ( 'NONE',  ( 0.000000000000000000, -1.000000000000000000, 0.000000000000000000 ) ) ;
#9411=DIRECTION ( 'NONE',  ( -0.9998748951565024079, 0.000000000000000000, -0.01581752306063006000 ) ) ;
#9681=CARTESIAN_POINT ( 'NONE',  ( -0.5999999999999999778, -5.000000000000000000, 4.000000000000000000 ) ) ;
#9735=VECTOR ( 'NONE', #17432, 1000.000000000000000 ) ;
#9778=EDGE_CURVE ( 'NONE', #13032, #29661, #32154, .T. ) ;
#9786=CARTESIAN_POINT ( 'NONE',  ( 4.000000000000000000, -5.200000000000000178, -0.5999999999999999778 ) ) ;
#9836=ORIENTED_EDGE ( 'NONE', *, *, #47931, .T. ) ;
#9872=FACE_BOUND ( 'NONE', #57957, .T. ) ;
#9873=PLANE ( 'NONE',  #50932 ) ;
#9968=DIRECTION ( 'NONE',  ( 1.000000000000000000, 0.000000000000000000, -0.000000000000000000 ) ) ;
#10015=( LENGTH_UNIT ( ) NAMED_UNIT ( * ) SI_UNIT ( .MILLI., .METRE. ) );
#10090=ORIENTED_EDGE ( 'NONE', *, *, #29266, .F. ) ;
#10156=DIRECTION ( 'NONE',  ( 0.000000000000000000, 0.000000000000000000, 1.000000000000000000 ) ) ;
#10167=CARTESIAN_POINT ( 'NONE',  ( 0.000000000000000000, -73.00000000000001421, 0.000000000000000000 ) ) ;
#10175=DIRECTION ( 'NONE',  ( -1.000000000000000000, 0.000000000000000000, 0.000000000000000000 ) ) ;
#10227=ORIENTED_EDGE ( 'NONE', *, *, #33846, .T. ) ;
#10451=ORIENTED_EDGE ( 'NONE', *, *, #12741, .F. ) ;
#10547=CARTESIAN_POINT ( 'NONE',  ( 0.000000000000000000, -75.00000000000001421, 0.000000000000000000 ) ) ;
#10554=SURFACE_STYLE_FILL_AREA ( #2853 ) ;
#10597=AXIS2_PLACEMENT_3D ( 'NONE', #22384, #45428, #22080 ) ;
#10664=CARTESIAN_POINT ( 'NONE',  ( -0.5999999999999999778, -5.000000000000000000, 4.000000000000000000 ) ) ;
#10694=ADVANCED_FACE ( 'NONE', ( #35879 ), #22603, .F. ) ;
#10795=CARTESIAN_POINT ( 'NONE',  ( 4.000000000000000000, -75.00000000000001421, 0.5999999999999999778 ) ) ;
#10798=VECTOR ( 'NONE', #27946, 1000.000000000000000 ) ;
#10957=PRODUCT_DEFINITION ( 'UNKNOWN', '', #4669, #26258 ) ;
#11026=VECTOR ( 'NONE', #21522, 1000.000000000000000 ) ;
#11048=VERTEX_POINT ( 'NONE', #43820 ) ;
#11110=CIRCLE ( 'NONE', #38438, 10.50000000000000000 ) ;
#11123=ORIENTED_EDGE ( 'NONE', *, *, #51904, .T. ) ;
#11183=VERTEX_POINT ( 'NONE', #35207 ) ;
#11256=AXIS2_PLACEMENT_3D ( 'NONE', #35576, #17290, #18185 ) ;
#11341=COLOUR_RGB ( '', 0.09019608, 0.27058824, 0.51372549) ;
#11397=CARTESIAN_POINT ( 'NONE',  ( -0.5999999999999999778, -5.000000000000000000, -4.000000000000000000 ) ) ;
#11484=AXIS2_PLACEMENT_3D ( 'NONE', #13759, #9351, #44778 ) ;
#11612=ORIENTED_EDGE ( 'NONE', *, *, #24179, .T. ) ;
#11655=ORIENTED_EDGE ( 'NONE', *, *, #54684, .T. ) ;
#11797=VECTOR ( 'NONE', #37641, 1000.000000000000000 ) ;
#11982=LINE ( 'NONE', #18364, #5185 ) ;
#12073=EDGE_CURVE ( 'NONE', #39893, #53803, #34326, .T. ) ;
#12103=ORIENTED_EDGE ( 'NONE', *, *, #53036, .F. ) ;
#12104=ORIENTED_EDGE ( 'NONE', *, *, #56073, .F. ) ;
#12255=CYLINDRICAL_SURFACE ( 'NONE', #13137, 10.50000000000000000 ) ;
#12262=ORIENTED_EDGE ( 'NONE', *, *, #50295, .T. ) ;
#12346=CARTESIAN_POINT ( 'NONE',  ( -10.50000000000000000, -7.000000000000000000, 0.000000000000000000 ) ) ;
#12473=AXIS2_PLACEMENT_3D ( 'NONE', #4385, #45133, #36839 ) ;
#12514=DIRECTION ( 'NONE',  ( 1.000000000000000000, 0.000000000000000000, 0.000000000000000000 ) ) ;
#12602=ORIENTED_EDGE ( 'NONE', *, *, #21468, .F. ) ;
#12612=ORIENTED_EDGE ( 'NONE', *, *, #39116, .T. ) ;
#12633=AXIS2_PLACEMENT_3D ( 'NONE', #40425, #35987, #44558 ) ;
#12741=EDGE_CURVE ( 'NONE', #35302, #34134, #33165, .T. ) ;
#12858=EDGE_CURVE ( 'NONE', #34312, #11183, #48938, .T. ) ;
#12884=ORIENTED_EDGE ( 'NONE', *, *, #12858, .T. ) ;
#12905=VECTOR ( 'NONE', #28821, 1000.000000000000000 ) ;
#13032=VERTEX_POINT ( 'NONE', #22639 ) ;
#13058=PLANE ( 'NONE',  #35313 ) ;
#13064=DIRECTION ( 'NONE',  ( 1.000000000000000000, 0.000000000000000000, 0.000000000000000000 ) ) ;
#13078=DIRECTION ( 'NONE',  ( 0.000000000000000000, -1.000000000000000000, 0.000000000000000000 ) ) ;
#13083=VECTOR ( 'NONE', #27141, 1000.000000000000000 ) ;
#13109=DIRECTION ( 'NONE',  ( 0.000000000000000000, 0.000000000000000000, -1.000000000000000000 ) ) ;
#13115=ORIENTED_EDGE ( 'NONE', *, *, #51849, .T. ) ;
#13137=AXIS2_PLACEMENT_3D ( 'NONE', #30247, #35245, #48855 ) ;
#13215=ADVANCED_FACE ( 'NONE', ( #52702 ), #12255, .T. ) ;
#13245=ORIENTED_EDGE ( 'NONE', *, *, #21693, .F. ) ;
#13262=UNCERTAINTY_MEASURE_WITH_UNIT (LENGTH_MEASURE( 1.000000000000000082E-05 ), #3121, 'distance_accuracy_value', 'NONE');
#13427=ADVANCED_FACE ( 'NONE', ( #27565 ), #31698, .T. ) ;
#13451=VECTOR ( 'NONE', #12514, 1000.000000000000000 ) ;
#13452=SHAPE_REPRESENTATION ( 'Battery', ( #43526 ), #49207 ) ;
#13506=ADVANCED_FACE ( 'NONE', ( #50323 ), #9873, .F. ) ;
#13579=VERTEX_POINT ( 'NONE', #15464 ) ;
#13614=DIRECTION ( 'NONE',  ( 0.000000000000000000, 0.000000000000000000, -1.000000000000000000 ) ) ;
#13616=ADVANCED_FACE ( 'NONE', ( #15748 ), #33911, .T. ) ;
#13689=EDGE_LOOP ( 'NONE', ( #10227, #13245, #7825, #20708 ) ) ;
#13701=ORIENTED_EDGE ( 'NONE', *, *, #50470, .F. ) ;
#13759=CARTESIAN_POINT ( 'NONE',  ( 0.000000000000000000, -7.000000000000000000, 0.000000000000000000 ) ) ;
#13803=AXIS2_PLACEMENT_3D ( 'NONE', #41893, #50181, #15020 ) ;
#14074=DIRECTION ( 'NONE',  ( 0.000000000000000000, 0.000000000000000000, 1.000000000000000000 ) ) ;
#14136=CIRCLE ( 'NONE', #34860, 8.500000000000000000 ) ;
#14197=LINE ( 'NONE', #18354, #22674 ) ;
#14310=CARTESIAN_POINT ( 'NONE',  ( 4.000000000000000000, -75.00000000000001421, -0.5999999999999999778 ) ) ;
#14340=ORIENTED_EDGE ( 'NONE', *, *, #37078, .F. ) ;
#14358=AXIS2_PLACEMENT_3D ( 'NONE', #5585, #50191, #50778 ) ;
#14442=AXIS2_PLACEMENT_3D ( 'NONE', #6632, #38209, #43517 ) ;
#14461=AXIS2_PLACEMENT_3D ( 'NONE', #9681, #19705, #28545 ) ;
#14564=DIRECTION ( 'NONE',  ( 1.000000000000000000, 0.000000000000000000, 0.000000000000000000 ) ) ;
#14587=EDGE_CURVE ( 'NONE', #11048, #8218, #8996, .T. ) ;
#14643=VECTOR ( 'NONE', #15118, 1000.000000000000000 ) ;
#14666=FACE_OUTER_BOUND ( 'NONE', #13689, .T. ) ;
#14698=ADVANCED_FACE ( 'NONE', ( #9872, #50032 ), #54160, .F. ) ;
#14704=EDGE_LOOP ( 'NONE', ( #32808, #16049, #47723, #30880 ) ) ;
#14710=( NAMED_UNIT ( * ) SI_UNIT ( $, .STERADIAN. ) SOLID_ANGLE_UNIT ( ) );
#14726=ORIENTED_EDGE ( 'NONE', *, *, #55099, .F. ) ;
#14739=AXIS2_PLACEMENT_3D ( 'NONE', #49474, #53902, #777 ) ;
#14780=ORIENTED_EDGE ( 'NONE', *, *, #43056, .T. ) ;
#14990=FACE_OUTER_BOUND ( 'NONE', #36686, .T. ) ;
#15020=DIRECTION ( 'NONE',  ( 1.000000000000000000, 0.000000000000000000, 0.000000000000000000 ) ) ;
#15118=DIRECTION ( 'NONE',  ( 0.000000000000000000, -1.000000000000000000, 0.000000000000000000 ) ) ;
#15162=SHAPE_DEFINITION_REPRESENTATION ( #17268, #13452 ) ;
#15356=CARTESIAN_POINT ( 'NONE',  ( 0.5999999999999999778, -5.000000000000000000, 0.5999999999999999778 ) ) ;
#15464=CARTESIAN_POINT ( 'NONE',  ( 0.5999999999999999778, -5.200000000000000178, -0.5999999999999999778 ) ) ;
#15472=CARTESIAN_POINT ( 'NONE',  ( 4.000000000000000000, -75.00000000000001421, 0.5999999999999999778 ) ) ;
#15523=LINE ( 'NONE', #51552, #23729 ) ;
#15584=CARTESIAN_POINT ( 'NONE',  ( -0.5999999999999999778, -5.000000000000000000, -4.000000000000000000 ) ) ;
#15610=FACE_OUTER_BOUND ( 'NONE', #36000, .T. ) ;
#15748=FACE_OUTER_BOUND ( 'NONE', #16464, .T. ) ;
#15849=PRESENTATION_STYLE_ASSIGNMENT (( #46585 ) ) ;
#15872=LINE ( 'NONE', #55742, #2950 ) ;
#15953=CARTESIAN_POINT ( 'NONE',  ( 0.5999999999999999778, -5.200000000000000178, -0.5999999999999999778 ) ) ;
#15980=LINE ( 'NONE', #2128, #24750 ) ;
#16049=ORIENTED_EDGE ( 'NONE', *, *, #36427, .F. ) ;
#16103=DIRECTION ( 'NONE',  ( 0.9999380042107527400, 0.000000000000000000, -0.01113497799803945566 ) ) ;
#16126=DIRECTION ( 'NONE',  ( 0.000000000000000000, -1.000000000000000000, 0.000000000000000000 ) ) ;
#16142=( NAMED_UNIT ( * ) SI_UNIT ( $, .STERADIAN. ) SOLID_ANGLE_UNIT ( ) );
#16219=CARTESIAN_POINT ( 'NONE',  ( -4.000000000000000000, -74.80000000000001137, -0.5999999999999999778 ) ) ;
#16331=ORIENTED_EDGE ( 'NONE', *, *, #24179, .F. ) ;
#16335=ORIENTED_EDGE ( 'NONE', *, *, #25379, .T. ) ;
#16410=EDGE_LOOP ( 'NONE', ( #18599, #38691, #2258, #28798 ) ) ;
#16464=EDGE_LOOP ( 'NONE', ( #34381, #42544, #52350, #42751 ) ) ;
#16760=ADVANCED_FACE ( 'NONE', ( #37241 ), #5949, .F. ) ;
#16761=DIRECTION ( 'NONE',  ( 0.000000000000000000, -1.000000000000000000, 0.000000000000000000 ) ) ;
#16873=LINE ( 'NONE', #34853, #5302 ) ;
#16916=ORIENTED_EDGE ( 'NONE', *, *, #47656, .T. ) ;
#16928=EDGE_LOOP ( 'NONE', ( #13115, #50530, #50895, #5831 ) ) ;
#17153=ORIENTED_EDGE ( 'NONE', *, *, #29293, .T. ) ;
#17207=FACE_OUTER_BOUND ( 'NONE', #23429, .T. ) ;
#17211=CARTESIAN_POINT ( 'NONE',  ( 0.000000000000000000, -7.000000000000000000, 0.000000000000000000 ) ) ;
#17268=PRODUCT_DEFINITION_SHAPE ( 'NONE', 'NONE',  #10957 ) ;
#17290=DIRECTION ( 'NONE',  ( 0.000000000000000000, 0.000000000000000000, 1.000000000000000000 ) ) ;
#17342=VECTOR ( 'NONE', #38793, 1000.000000000000000 ) ;
#17432=DIRECTION ( 'NONE',  ( 0.000000000000000000, 1.000000000000000000, 0.000000000000000000 ) ) ;
#17806=CARTESIAN_POINT ( 'NONE',  ( -0.5999999999999999778, -5.200000000000000178, -0.5999999999999999778 ) ) ;
#17854=DIRECTION ( 'NONE',  ( 0.000000000000000000, -1.000000000000000000, 0.000000000000000000 ) ) ;
#17914=EDGE_CURVE ( 'NONE', #31619, #34639, #46006, .T. ) ;
#18185=DIRECTION ( 'NONE',  ( 1.000000000000000000, 0.000000000000000000, 0.000000000000000000 ) ) ;
#18340=DIRECTION ( 'NONE',  ( 0.000000000000000000, 0.000000000000000000, 1.000000000000000000 ) ) ;
#18354=CARTESIAN_POINT ( 'NONE',  ( 0.5999999999999999778, -5.200000000000000178, 4.000000000000000000 ) ) ;
#18356=CARTESIAN_POINT ( 'NONE',  ( 0.000000000000000000, -73.00000000000001421, 0.000000000000000000 ) ) ;
#18364=CARTESIAN_POINT ( 'NONE',  ( -0.5999999999999999778, -5.000000000000000000, 0.5999999999999999778 ) ) ;
#18427=ADVANCED_FACE ( 'NONE', ( #18468 ), #45636, .F. ) ;
#18468=FACE_OUTER_BOUND ( 'NONE', #24397, .T. ) ;
#18570=EDGE_CURVE ( 'NONE', #25098, #21810, #28467, .T. ) ;
#18599=ORIENTED_EDGE ( 'NONE', *, *, #57675, .T. ) ;
#18657=LINE ( 'NONE', #23067, #34203 ) ;
#18738=CARTESIAN_POINT ( 'NONE',  ( -4.000000000000000000, -75.00000000000001421, 0.5999999999999999778 ) ) ;
#18939=ORIENTED_EDGE ( 'NONE', *, *, #47656, .F. ) ;
#18971=AXIS2_PLACEMENT_3D ( 'NONE', #1539, #19531, #28666 ) ;
#19018=TOROIDAL_SURFACE ( 'NONE', #11484, 8.500000000000000000, 2.000000000000000000 ) ;
#19091=CARTESIAN_POINT ( 'NONE',  ( 4.000000000000000000, -5.200000000000000178, 0.5999999999999999778 ) ) ;
#19155=EDGE_CURVE ( 'NONE', #57897, #22013, #30993, .T. ) ;
#19160=FILL_AREA_STYLE_COLOUR ( '', #56759 ) ;
#19195=DIRECTION ( 'NONE',  ( 0.000000000000000000, 0.000000000000000000, -1.000000000000000000 ) ) ;
#19378=EDGE_CURVE ( 'NONE', #34134, #13032, #41167, .T. ) ;
#19519=EDGE_LOOP ( 'NONE', ( #6575, #41345, #45752, #12104 ) ) ;
#19531=DIRECTION ( 'NONE',  ( 0.000000000000000000, -1.000000000000000000, 0.000000000000000000 ) ) ;
#19554=LINE ( 'NONE', #23108, #14643 ) ;
#19705=DIRECTION ( 'NONE',  ( 0.000000000000000000, 0.000000000000000000, 1.000000000000000000 ) ) ;
#19844=ORIENTED_EDGE ( 'NONE', *, *, #9778, .F. ) ;
#19998=( LENGTH_UNIT ( ) NAMED_UNIT ( * ) SI_UNIT ( .MILLI., .METRE. ) );
#20127=UNCERTAINTY_MEASURE_WITH_UNIT (LENGTH_MEASURE( 1.000000000000000082E-05 ), #10015, 'distance_accuracy_value', 'NONE');
#20220=FACE_OUTER_BOUND ( 'NONE', #16928, .T. ) ;
#20255=ORIENTED_EDGE ( 'NONE', *, *, #46971, .T. ) ;
#20372=CARTESIAN_POINT ( 'NONE',  ( -8.500000000000000000, -7.000000000000000000, 0.000000000000000000 ) ) ;
#20421=DIRECTION ( 'NONE',  ( 0.000000000000000000, 1.000000000000000000, 0.000000000000000000 ) ) ;
#20634=VERTEX_POINT ( 'NONE', #39112 ) ;
#20708=ORIENTED_EDGE ( 'NONE', *, *, #35264, .T. ) ;
#20885=ORIENTED_EDGE ( 'NONE', *, *, #43896, .T. ) ;
#21090=AXIS2_PLACEMENT_3D ( 'NONE', #43967, #48404, #40103 ) ;
#21336=CARTESIAN_POINT ( 'NONE',  ( -0.5999999999999999778, -5.000000000000000000, -4.000000000000000000 ) ) ;
#21338=EDGE_CURVE ( 'NONE', #21810, #33522, #11110, .T. ) ;
#21400=DIRECTION ( 'NONE',  ( 0.000000000000000000, 0.000000000000000000, 1.000000000000000000 ) ) ;
#21420=EDGE_CURVE ( 'NONE', #36179, #13579, #50822, .T. ) ;
#21468=EDGE_CURVE ( 'NONE', #51903, #46323, #24327, .T. ) ;
#21522=DIRECTION ( 'NONE',  ( 1.000000000000000000, 0.000000000000000000, 0.000000000000000000 ) ) ;
#21599=MECHANICAL_DESIGN_GEOMETRIC_PRESENTATION_REPRESENTATION('',(#46405),#50873);
#21693=EDGE_CURVE ( 'NONE', #13579, #51686, #25670, .T. ) ;
#21810=VERTEX_POINT ( 'NONE', #5792 ) ;
#21894=ORIENTED_EDGE ( 'NONE', *, *, #36182, .T. ) ;
#22013=VERTEX_POINT ( 'NONE', #19091 ) ;
#22080=DIRECTION ( 'NONE',  ( 1.000000000000000000, 0.000000000000000000, 0.000000000000000000 ) ) ;
#22082=CARTESIAN_POINT ( 'NONE',  ( -4.000000000000000000, -75.00000000000001421, -0.5999999999999999778 ) ) ;
#22214=VERTEX_POINT ( 'NONE', #32717 ) ;
#22384=CARTESIAN_POINT ( 'NONE',  ( 0.000000000000000000, -73.00000000000001421, 0.000000000000000000 ) ) ;
#22411=ORIENTED_EDGE ( 'NONE', *, *, #50295, .F. ) ;
#22463=LINE ( 'NONE', #361, #23638 ) ;
#22539=CARTESIAN_POINT ( 'NONE',  ( -4.000000000000000000, -5.200000000000000178, 0.5999999999999999778 ) ) ;
#22603=PLANE ( 'NONE',  #11256 ) ;
#22633=VERTEX_POINT ( 'NONE', #52117 ) ;
#22639=CARTESIAN_POINT ( 'NONE',  ( -4.000000000000000000, -75.00000000000001421, -0.5999999999999999778 ) ) ;
#22648=CARTESIAN_POINT ( 'NONE',  ( -4.000000000000000000, -5.000000000000000000, 0.5999999999999999778 ) ) ;
#22674=VECTOR ( 'NONE', #13614, 1000.000000000000000 ) ;
#22699=VERTEX_POINT ( 'NONE', #52976 ) ;
#22729=CYLINDRICAL_SURFACE ( 'NONE', #14358, 10.50000000000000000 ) ;
#22879=CARTESIAN_POINT ( 'NONE',  ( 4.000000000000000000, -75.00000000000001421, 0.5999999999999999778 ) ) ;
#22923=ORIENTED_EDGE ( 'NONE', *, *, #47931, .F. ) ;
#23067=CARTESIAN_POINT ( 'NONE',  ( -0.5999999999999999778, -5.000000000000000000, 0.5999999999999999778 ) ) ;
#23078=EDGE_LOOP ( 'NONE', ( #26628, #46484, #19844, #26458 ) ) ;
#23108=CARTESIAN_POINT ( 'NONE',  ( 4.000000000000000000, -5.000000000000000000, 0.5999999999999999778 ) ) ;
#23150=DIRECTION ( 'NONE',  ( 1.000000000000000000, 0.000000000000000000, 0.000000000000000000 ) ) ;
#23278=ORIENTED_EDGE ( 'NONE', *, *, #25379, .F. ) ;
#23287=EDGE_LOOP ( 'NONE', ( #3311, #56620, #34234, #1456 ) ) ;
#23429=EDGE_LOOP ( 'NONE', ( #4871, #17153 ) ) ;
#23570=EDGE_CURVE ( 'NONE', #51903, #33522, #35557, .T. ) ;
#23610=CARTESIAN_POINT ( 'NONE',  ( -4.000000000000000000, -74.80000000000001137, 0.5999999999999999778 ) ) ;
#23637=LINE ( 'NONE', #41363, #43079 ) ;
#23638=VECTOR ( 'NONE', #18340, 1000.000000000000000 ) ;
#23665=CARTESIAN_POINT ( 'NONE',  ( 0.5999999999999999778, -5.000000000000000000, 4.000000000000000000 ) ) ;
#23729=VECTOR ( 'NONE', #32627, 1000.000000000000000 ) ;
#23784=VECTOR ( 'NONE', #24669, 1000.000000000000000 ) ;
#23816=DIRECTION ( 'NONE',  ( 0.000000000000000000, -1.000000000000000000, 0.000000000000000000 ) ) ;
#23823=CARTESIAN_POINT ( 'NONE',  ( 0.5999999999999999778, -5.000000000000000000, -0.5999999999999999778 ) ) ;
#23887=FACE_OUTER_BOUND ( 'NONE', #31837, .T. ) ;
#23902=VECTOR ( 'NONE', #50507, 1000.000000000000000 ) ;
#23965=VERTEX_POINT ( 'NONE', #22539 ) ;
#24049=CARTESIAN_POINT ( 'NONE',  ( -10.50000000000000000, -7.000000000000000000, -5.990939290788000838E-12 ) ) ;
#24113=DIRECTION ( 'NONE',  ( -1.000000000000000000, 0.000000000000000000, 0.000000000000000000 ) ) ;
#24179=EDGE_CURVE ( 'NONE', #45504, #23965, #45205, .T. ) ;
#24234=CARTESIAN_POINT ( 'NONE',  ( 0.000000000000000000, -75.00000000000001421, 0.000000000000000000 ) ) ;
#24327=CIRCLE ( 'NONE', #45063, 8.500000000000000000 ) ;
#24379=AXIS2_PLACEMENT_3D ( 'NONE', #23665, #31927, #4796 ) ;
#24397=EDGE_LOOP ( 'NONE', ( #11655, #30502, #49065, #6222 ) ) ;
#24533=AXIS2_PLACEMENT_3D ( 'NONE', #27275, #17854, #23150 ) ;
#24607=ORIENTED_EDGE ( 'NONE', *, *, #42437, .F. ) ;
#24617=ORIENTED_EDGE ( 'NONE', *, *, #9778, .T. ) ;
#24668=DIRECTION ( 'NONE',  ( 0.000000000000000000, -1.000000000000000000, 0.000000000000000000 ) ) ;
#24669=DIRECTION ( 'NONE',  ( -1.000000000000000000, 0.000000000000000000, 0.000000000000000000 ) ) ;
#24674=ORIENTED_EDGE ( 'NONE', *, *, #19378, .F. ) ;
#24717=FACE_OUTER_BOUND ( 'NONE', #39691, .T. ) ;
#24750=VECTOR ( 'NONE', #56140, 1000.000000000000000 ) ;
#24804=CARTESIAN_POINT ( 'NONE',  ( 0.5999999999999999778, -5.200000000000000178, 4.000000000000000000 ) ) ;
#24887=ORIENTED_EDGE ( 'NONE', *, *, #9038, .F. ) ;
#24916=AXIS2_PLACEMENT_3D ( 'NONE', #15584, #28566, #27980 ) ;
#25098=VERTEX_POINT ( 'NONE', #12346 ) ;
#25196=CARTESIAN_POINT ( 'NONE',  ( 4.000000000000000000, -5.000000000000000000, -0.5999999999999999778 ) ) ;
#25379=EDGE_CURVE ( 'NONE', #29440, #11048, #23637, .T. ) ;
#25472=EDGE_CURVE ( 'NONE', #2048, #22633, #51110, .T. ) ;
#25478=DIRECTION ( 'NONE',  ( 0.000000000000000000, -1.000000000000000000, 0.000000000000000000 ) ) ;
#25482=FACE_OUTER_BOUND ( 'NONE', #51499, .T. ) ;
#25495=AXIS2_PLACEMENT_3D ( 'NONE', #37427, #49867, #9411 ) ;
#25599=ORIENTED_EDGE ( 'NONE', *, *, #21420, .F. ) ;
#25650=DIRECTION ( 'NONE',  ( 0.000000000000000000, 0.000000000000000000, 1.000000000000000000 ) ) ;
#25670=LINE ( 'NONE', #15953, #39404 ) ;
#25748=EDGE_CURVE ( 'NONE', #25098, #22699, #36446, .T. ) ;
#25753=ORIENTED_EDGE ( 'NONE', *, *, #4722, .T. ) ;
#25817=EDGE_CURVE ( 'NONE', #23965, #20634, #43811, .T. ) ;
#25925=CARTESIAN_POINT ( 'NONE',  ( -4.000000000000000000, -74.80000000000001137, 0.5999999999999999778 ) ) ;
#26106=EDGE_CURVE ( 'NONE', #22699, #33522, #53824, .T. ) ;
#26199=CARTESIAN_POINT ( 'NONE',  ( 4.000000000000000000, -74.80000000000001137, -0.5999999999999999778 ) ) ;
#26258=PRODUCT_DEFINITION_CONTEXT ( 'detailed design', #36048, 'design' ) ;
#26285=LINE ( 'NONE', #57875, #9735 ) ;
#26355=DIRECTION ( 'NONE',  ( 0.000000000000000000, 0.000000000000000000, -1.000000000000000000 ) ) ;
#26458=ORIENTED_EDGE ( 'NONE', *, *, #37078, .T. ) ;
#26628=ORIENTED_EDGE ( 'NONE', *, *, #7631, .T. ) ;
#26763=CARTESIAN_POINT ( 'NONE',  ( -4.000000000000000000, -5.000000000000000000, -0.5999999999999999778 ) ) ;
#26955=EDGE_CURVE ( 'NONE', #2048, #670, #16873, .T. ) ;
#26977=DIRECTION ( 'NONE',  ( 0.000000000000000000, -1.000000000000000000, 0.000000000000000000 ) ) ;
#27141=DIRECTION ( 'NONE',  ( 0.000000000000000000, 1.000000000000000000, 0.000000000000000000 ) ) ;
#27162=VERTEX_POINT ( 'NONE', #25925 ) ;
#27275=CARTESIAN_POINT ( 'NONE',  ( 0.000000000000000000, -5.000000000000000000, 0.000000000000000000 ) ) ;
#27448=CARTESIAN_POINT ( 'NONE',  ( 4.000000000000000000, -75.00000000000001421, -0.5999999999999999778 ) ) ;
#27563=CARTESIAN_POINT ( 'NONE',  ( -4.000000000000000000, -5.000000000000000000, -0.5999999999999999778 ) ) ;
#27565=FACE_OUTER_BOUND ( 'NONE', #44482, .T. ) ;
#27669=DIRECTION ( 'NONE',  ( 0.000000000000000000, 0.000000000000000000, -1.000000000000000000 ) ) ;
#27773=DIRECTION ( 'NONE',  ( 1.000000000000000000, 0.000000000000000000, 0.000000000000000000 ) ) ;
#27946=DIRECTION ( 'NONE',  ( 0.000000000000000000, -1.000000000000000000, 0.000000000000000000 ) ) ;
#27980=DIRECTION ( 'NONE',  ( 0.000000000000000000, -1.000000000000000000, 0.000000000000000000 ) ) ;
#28200=CARTESIAN_POINT ( 'NONE',  ( 8.500000000000000000, -75.00000000000001421, 0.000000000000000000 ) ) ;
#28245=PLANE ( 'NONE',  #14461 ) ;
#28254=ORIENTED_EDGE ( 'NONE', *, *, #29266, .T. ) ;
#28268=DIRECTION ( 'NONE',  ( 0.000000000000000000, -1.000000000000000000, 0.000000000000000000 ) ) ;
#28284=( NAMED_UNIT ( * ) PLANE_ANGLE_UNIT ( ) SI_UNIT ( $, .RADIAN. ) );
#28341=ADVANCED_FACE ( 'NONE', ( #15610 ), #41310, .F. ) ;
#28467=LINE ( 'NONE', #24049, #9107 ) ;
#28537=SURFACE_SIDE_STYLE ('',( #10554 ) ) ;
#28545=DIRECTION ( 'NONE',  ( 1.000000000000000000, 0.000000000000000000, 0.000000000000000000 ) ) ;
#28548=CARTESIAN_POINT ( 'NONE',  ( 8.500000000000000000, -73.00000000000001421, 0.000000000000000000 ) ) ;
#28566=DIRECTION ( 'NONE',  ( -1.000000000000000000, 0.000000000000000000, 0.000000000000000000 ) ) ;
#28666=DIRECTION ( 'NONE',  ( 1.000000000000000000, 0.000000000000000000, 0.000000000000000000 ) ) ;
#28798=ORIENTED_EDGE ( 'NONE', *, *, #12741, .T. ) ;
#28821=DIRECTION ( 'NONE',  ( -1.000000000000000000, 0.000000000000000000, 0.000000000000000000 ) ) ;
#28834=CARTESIAN_POINT ( 'NONE',  ( 4.000000000000000000, -5.000000000000000000, 0.5999999999999999778 ) ) ;
#29089=CARTESIAN_POINT ( 'NONE',  ( 0.5999999999999999778, -5.200000000000000178, 0.5999999999999999778 ) ) ;
#29090=CARTESIAN_POINT ( 'NONE',  ( 4.000000000000000000, -5.000000000000000000, -0.5999999999999999778 ) ) ;
#29138=DIRECTION ( 'NONE',  ( -1.000000000000000000, 0.000000000000000000, 0.000000000000000000 ) ) ;
#29266=EDGE_CURVE ( 'NONE', #22214, #55898, #38990, .T. ) ;
#29293=EDGE_CURVE ( 'NONE', #46323, #51903, #45954, .T. ) ;
#29389=ORIENTED_EDGE ( 'NONE', *, *, #17914, .F. ) ;
#29421=CIRCLE ( 'NONE', #21090, 10.50000000000000000 ) ;
#29440=VERTEX_POINT ( 'NONE', #34409 ) ;
#29661=VERTEX_POINT ( 'NONE', #50057 ) ;
#29673=DIRECTION ( 'NONE',  ( 0.000000000000000000, -1.000000000000000000, 0.000000000000000000 ) ) ;
#29679=PLANE ( 'NONE',  #39051 ) ;
#29790=PLANE ( 'NONE',  #38306 ) ;
#29950=ORIENTED_EDGE ( 'NONE', *, *, #6764, .T. ) ;
#29953=PRESENTATION_STYLE_ASSIGNMENT (( #52703 ) ) ;
#30072=AXIS2_PLACEMENT_3D ( 'NONE', #35542, #31992, #13109 ) ;
#30084=ORIENTED_EDGE ( 'NONE', *, *, #56073, .T. ) ;
#30169=EDGE_LOOP ( 'NONE', ( #30879, #39178, #16331, #12262 ) ) ;
#30205=PLANE ( 'NONE',  #14442 ) ;
#30247=CARTESIAN_POINT ( 'NONE',  ( 0.000000000000000000, -5.000000000000000000, 0.000000000000000000 ) ) ;
#30368=ORIENTED_EDGE ( 'NONE', *, *, #52639, .F. ) ;
#30462=ORIENTED_EDGE ( 'NONE', *, *, #26955, .F. ) ;
#30502=ORIENTED_EDGE ( 'NONE', *, *, #12858, .F. ) ;
#30637=DIRECTION ( 'NONE',  ( 1.000000000000000000, 0.000000000000000000, 0.000000000000000000 ) ) ;
#30771=DIRECTION ( 'NONE',  ( 0.000000000000000000, -1.000000000000000000, 0.000000000000000000 ) ) ;
#30834=AXIS2_PLACEMENT_3D ( 'NONE', #28548, #37706, #54562 ) ;
#30879=ORIENTED_EDGE ( 'NONE', *, *, #31426, .T. ) ;
#30880=ORIENTED_EDGE ( 'NONE', *, *, #4441, .T. ) ;
#30993=LINE ( 'NONE', #31579, #50637 ) ;
#31057=DIRECTION ( 'NONE',  ( 1.000000000000000000, 0.000000000000000000, 0.000000000000000000 ) ) ;
#31161=VECTOR ( 'NONE', #45394, 1000.000000000000000 ) ;
#31235=VECTOR ( 'NONE', #32294, 1000.000000000000000 ) ;
#31246=FACE_OUTER_BOUND ( 'NONE', #43120, .T. ) ;
#31426=EDGE_CURVE ( 'NONE', #52567, #20634, #11982, .T. ) ;
#31468=ORIENTED_EDGE ( 'NONE', *, *, #52639, .T. ) ;
#31545=PLANE ( 'NONE',  #12633 ) ;
#31579=CARTESIAN_POINT ( 'NONE',  ( 0.5999999999999999778, -5.200000000000000178, 0.5999999999999999778 ) ) ;
#31619=VERTEX_POINT ( 'NONE', #53419 ) ;
#31695=CARTESIAN_POINT ( 'NONE',  ( 0.5999999999999999778, -5.000000000000000000, 4.000000000000000000 ) ) ;
#31698=PLANE ( 'NONE',  #30072 ) ;
#31837=EDGE_LOOP ( 'NONE', ( #44378, #6088, #6001, #40349 ) ) ;
#31887=CARTESIAN_POINT ( 'NONE',  ( -4.000000000000000000, -5.000000000000000000, 0.5999999999999999778 ) ) ;
#31911=DIRECTION ( 'NONE',  ( 0.000000000000000000, 0.000000000000000000, 1.000000000000000000 ) ) ;
#31927=DIRECTION ( 'NONE',  ( 1.000000000000000000, 0.000000000000000000, -0.000000000000000000 ) ) ;
#31961=DIRECTION ( 'NONE',  ( 0.000000000000000000, 0.000000000000000000, -1.000000000000000000 ) ) ;
#31992=DIRECTION ( 'NONE',  ( 0.000000000000000000, 1.000000000000000000, 0.000000000000000000 ) ) ;
#32154=LINE ( 'NONE', #44580, #13083 ) ;
#32294=DIRECTION ( 'NONE',  ( 0.000000000000000000, 1.000000000000000000, 0.000000000000000000 ) ) ;
#32359=VECTOR ( 'NONE', #29138, 1000.000000000000000 ) ;
#32622=CARTESIAN_POINT ( 'NONE',  ( -0.5999999999999999778, -5.200000000000000178, -0.5999999999999999778 ) ) ;
#32627=DIRECTION ( 'NONE',  ( 1.000000000000000000, 0.000000000000000000, 0.000000000000000000 ) ) ;
#32697=DIRECTION ( 'NONE',  ( -1.000000000000000000, 0.000000000000000000, 0.000000000000000000 ) ) ;
#32717=CARTESIAN_POINT ( 'NONE',  ( 4.000000000000000000, -5.000000000000000000, -0.5999999999999999778 ) ) ;
#32808=ORIENTED_EDGE ( 'NONE', *, *, #12073, .T. ) ;
#33165=LINE ( 'NONE', #15472, #7515 ) ;
#33330=CIRCLE ( 'NONE', #7882, 2.000000000000000000 ) ;
#33511=LINE ( 'NONE', #32622, #23784 ) ;
#33522=VERTEX_POINT ( 'NONE', #43570 ) ;
#33707=EDGE_LOOP ( 'NONE', ( #56390, #30084 ) ) ;
#33732=ADVANCED_FACE ( 'NONE', ( #44151 ), #29679, .F. ) ;
#33846=EDGE_CURVE ( 'NONE', #1255, #51686, #1413, .T. ) ;
#33852=LINE ( 'NONE', #48050, #32359 ) ;
#33858=DIRECTION ( 'NONE',  ( 0.000000000000000000, 0.000000000000000000, -1.000000000000000000 ) ) ;
#33860=ORIENTED_EDGE ( 'NONE', *, *, #21693, .T. ) ;
#33911=TOROIDAL_SURFACE ( 'NONE', #5644, 8.500000000000000000, 2.000000000000000000 ) ;
#34124=ADVANCED_FACE ( 'NONE', ( #4219, #17207 ), #13058, .T. ) ;
#34134=VERTEX_POINT ( 'NONE', #52373 ) ;
#34162=CIRCLE ( 'NONE', #10597, 10.50000000000000000 ) ;
#34203=VECTOR ( 'NONE', #31911, 1000.000000000000000 ) ;
#34234=ORIENTED_EDGE ( 'NONE', *, *, #18570, .T. ) ;
#34312=VERTEX_POINT ( 'NONE', #40748 ) ;
#34326=LINE ( 'NONE', #21336, #47072 ) ;
#34337=CARTESIAN_POINT ( 'NONE',  ( 0.000000000000000000, -75.00000000000001421, 0.000000000000000000 ) ) ;
#34359=CARTESIAN_POINT ( 'NONE',  ( 0.5999999999999999778, -5.000000000000000000, 0.5999999999999999778 ) ) ;
#34378=AXIS2_PLACEMENT_3D ( 'NONE', #34662, #24668, #16103 ) ;
#34381=ORIENTED_EDGE ( 'NONE', *, *, #9038, .T. ) ;
#34409=CARTESIAN_POINT ( 'NONE',  ( -0.5999999999999999778, -5.000000000000000000, -0.5999999999999999778 ) ) ;
#34639=VERTEX_POINT ( 'NONE', #57961 ) ;
#34662=CARTESIAN_POINT ( 'NONE',  ( 0.000000000000000000, -73.00000000000001421, 0.000000000000000000 ) ) ;
#34667=VECTOR ( 'NONE', #55528, 1000.000000000000000 ) ;
#34788=LINE ( 'NONE', #22082, #4993 ) ;
#34853=CARTESIAN_POINT ( 'NONE',  ( -0.5999999999999999778, -5.000000000000000000, 4.000000000000000000 ) ) ;
#34860=AXIS2_PLACEMENT_3D ( 'NONE', #53361, #44221, #35336 ) ;
#34919=PLANE ( 'NONE',  #37073 ) ;
#35199=DIRECTION ( 'NONE',  ( 0.000000000000000000, 1.000000000000000000, 0.000000000000000000 ) ) ;
#35207=CARTESIAN_POINT ( 'NONE',  ( 4.000000000000000000, -74.80000000000001137, 0.5999999999999999778 ) ) ;
#35245=DIRECTION ( 'NONE',  ( 0.000000000000000000, -1.000000000000000000, 0.000000000000000000 ) ) ;
#35264=EDGE_CURVE ( 'NONE', #55898, #1255, #55363, .T. ) ;
#35302=VERTEX_POINT ( 'NONE', #10795 ) ;
#35313=AXIS2_PLACEMENT_3D ( 'NONE', #34337, #30771, #31057 ) ;
#35336=DIRECTION ( 'NONE',  ( 1.000000000000000000, 0.000000000000000000, 0.000000000000000000 ) ) ;
#35365=ORIENTED_EDGE ( 'NONE', *, *, #25748, .T. ) ;
#35529=ADVANCED_BREP_SHAPE_REPRESENTATION ( '', ( #56346, #43526 ), #49207 ) ;
#35536=VERTEX_POINT ( 'NONE', #24804 ) ;
#35542=CARTESIAN_POINT ( 'NONE',  ( 0.000000000000000000, -5.200000000000000178, 0.000000000000000000 ) ) ;
#35557=CIRCLE ( 'NONE', #30834, 2.000000000000001776 ) ;
#35576=CARTESIAN_POINT ( 'NONE',  ( -4.000000000000000000, -5.000000000000000000, 0.5999999999999999778 ) ) ;
#35877=EDGE_CURVE ( 'NONE', #42169, #35302, #4601, .T. ) ;
#35879=FACE_OUTER_BOUND ( 'NONE', #30169, .T. ) ;
#35987=DIRECTION ( 'NONE',  ( 0.000000000000000000, 0.000000000000000000, -1.000000000000000000 ) ) ;
#36000=EDGE_LOOP ( 'NONE', ( #21894, #37020, #40799, #14780 ) ) ;
#36032=CIRCLE ( 'NONE', #12473, 2.000000000000000000 ) ;
#36048=APPLICATION_CONTEXT ( 'automotive_design' ) ;
#36062=VECTOR ( 'NONE', #50484, 1000.000000000000000 ) ;
#36065=ORIENTED_EDGE ( 'NONE', *, *, #36427, .T. ) ;
#36179=VERTEX_POINT ( 'NONE', #41994 ) ;
#36182=EDGE_CURVE ( 'NONE', #39462, #22013, #19554, .T. ) ;
#36427=EDGE_CURVE ( 'NONE', #51686, #53803, #4374, .T. ) ;
#36446=CIRCLE ( 'NONE', #37414, 10.50000000000000000 ) ;
#36538=LINE ( 'NONE', #28834, #42763 ) ;
#36686=EDGE_LOOP ( 'NONE', ( #16916, #13701, #6383, #7753 ) ) ;
#36732=DIRECTION ( 'NONE',  ( 0.000000000000000000, 0.000000000000000000, -1.000000000000000000 ) ) ;
#36766=STYLED_ITEM ( 'NONE', ( #15849 ), #56346 ) ;
#36839=DIRECTION ( 'NONE',  ( 0.000000000000000000, 1.000000000000000000, 0.000000000000000000 ) ) ;
#36859=ORIENTED_EDGE ( 'NONE', *, *, #35264, .F. ) ;
#37020=ORIENTED_EDGE ( 'NONE', *, *, #19155, .F. ) ;
#37073=AXIS2_PLACEMENT_3D ( 'NONE', #49404, #26355, #52950 ) ;
#37078=EDGE_CURVE ( 'NONE', #13032, #42169, #34788, .T. ) ;
#37241=FACE_OUTER_BOUND ( 'NONE', #9203, .T. ) ;
#37414=AXIS2_PLACEMENT_3D ( 'NONE', #17211, #35199, #48248 ) ;
#37427=CARTESIAN_POINT ( 'NONE',  ( 0.000000000000000000, -7.000000000000000000, 0.000000000000000000 ) ) ;
#37641=DIRECTION ( 'NONE',  ( 0.000000000000000000, 0.000000000000000000, -1.000000000000000000 ) ) ;
#37706=DIRECTION ( 'NONE',  ( 0.000000000000000000, 0.000000000000000000, 1.000000000000000000 ) ) ;
#37802=VECTOR ( 'NONE', #42416, 1000.000000000000000 ) ;
#37875=CARTESIAN_POINT ( 'NONE',  ( -4.000000000000000000, -5.000000000000000000, 0.5999999999999999778 ) ) ;
#37967=LINE ( 'NONE', #1986, #37802 ) ;
#38209=DIRECTION ( 'NONE',  ( 1.000000000000000000, 0.000000000000000000, -0.000000000000000000 ) ) ;
#38306=AXIS2_PLACEMENT_3D ( 'NONE', #56687, #7376, #56970 ) ;
#38386=ORIENTED_EDGE ( 'NONE', *, *, #46924, .F. ) ;
#38406=UNCERTAINTY_MEASURE_WITH_UNIT (LENGTH_MEASURE( 1.000000000000000082E-05 ), #19998, 'distance_accuracy_value', 'NONE');
#38438=AXIS2_PLACEMENT_3D ( 'NONE', #18356, #49063, #40194 ) ;
#38454=CARTESIAN_POINT ( 'NONE',  ( 0.5999999999999999778, -5.000000000000000000, -0.5999999999999999778 ) ) ;
#38472=EDGE_CURVE ( 'NONE', #22699, #25098, #29421, .T. ) ;
#38506=CARTESIAN_POINT ( 'NONE',  ( -0.5999999999999999778, -5.000000000000000000, -4.000000000000000000 ) ) ;
#38626=ADVANCED_FACE ( 'NONE', ( #41576 ), #46029, .F. ) ;
#38665=AXIS2_PLACEMENT_3D ( 'NONE', #23823, #9968, #1127 ) ;
#38691=ORIENTED_EDGE ( 'NONE', *, *, #41284, .F. ) ;
#38704=DIRECTION ( 'NONE',  ( -1.000000000000000000, 0.000000000000000000, 0.000000000000000000 ) ) ;
#38793=DIRECTION ( 'NONE',  ( -1.000000000000000000, 0.000000000000000000, 0.000000000000000000 ) ) ;
#38990=LINE ( 'NONE', #57000, #12905 ) ;
#38996=CARTESIAN_POINT ( 'NONE',  ( 0.000000000000000000, -5.000000000000000000, 0.000000000000000000 ) ) ;
#39051=AXIS2_PLACEMENT_3D ( 'NONE', #2554, #57713, #16126 ) ;
#39112=CARTESIAN_POINT ( 'NONE',  ( -0.5999999999999999778, -5.200000000000000178, 0.5999999999999999778 ) ) ;
#39116=EDGE_CURVE ( 'NONE', #46485, #8218, #33511, .T. ) ;
#39178=ORIENTED_EDGE ( 'NONE', *, *, #25817, .F. ) ;
#39404=VECTOR ( 'NONE', #2106, 1000.000000000000000 ) ;
#39462=VERTEX_POINT ( 'NONE', #43974 ) ;
#39628=( GEOMETRIC_REPRESENTATION_CONTEXT ( 3 ) GLOBAL_UNCERTAINTY_ASSIGNED_CONTEXT ( ( #38406 ) ) GLOBAL_UNIT_ASSIGNED_CONTEXT ( ( #19998, #51875, #16142 ) ) REPRESENTATION_CONTEXT ( 'NONE', 'WORKASPACE' ) );
#39691=EDGE_LOOP ( 'NONE', ( #11612, #56118, #44544, #7580 ) ) ;
#39893=VERTEX_POINT ( 'NONE', #38506 ) ;
#40103=DIRECTION ( 'NONE',  ( 1.000000000000000000, 0.000000000000000000, 0.000000000000000000 ) ) ;
#40194=DIRECTION ( 'NONE',  ( -1.000000000000000000, 0.000000000000000000, 0.000000000000000000 ) ) ;
#40349=ORIENTED_EDGE ( 'NONE', *, *, #21338, .F. ) ;
#40385=PRODUCT ( 'Battery', 'Battery', '', ( #46197 ) ) ;
#40387=CARTESIAN_POINT ( 'NONE',  ( 0.5999999999999999778, -5.200000000000000178, -4.000000000000000000 ) ) ;
#40425=CARTESIAN_POINT ( 'NONE',  ( -0.5999999999999999778, -5.000000000000000000, -0.5999999999999999778 ) ) ;
#40568=ORIENTED_EDGE ( 'NONE', *, *, #51904, .F. ) ;
#40673=EDGE_CURVE ( 'NONE', #39462, #22214, #36538, .T. ) ;
#40692=ADVANCED_FACE ( 'NONE', ( #51012 ), #28245, .F. ) ;
#40748=CARTESIAN_POINT ( 'NONE',  ( 4.000000000000000000, -74.80000000000001137, -0.5999999999999999778 ) ) ;
#40799=ORIENTED_EDGE ( 'NONE', *, *, #41158, .F. ) ;
#40964=CARTESIAN_POINT ( 'NONE',  ( 0.5999999999999999778, -5.000000000000000000, -4.000000000000000000 ) ) ;
#41093=FACE_OUTER_BOUND ( 'NONE', #55988, .T. ) ;
#41158=EDGE_CURVE ( 'NONE', #2598, #57897, #55210, .T. ) ;
#41167=LINE ( 'NONE', #18738, #50681 ) ;
#41284=EDGE_CURVE ( 'NONE', #11183, #27162, #33852, .T. ) ;
#41310=PLANE ( 'NONE',  #13803 ) ;
#41340=CIRCLE ( 'NONE', #51722, 2.000000000000001776 ) ;
#41345=ORIENTED_EDGE ( 'NONE', *, *, #38472, .T. ) ;
#41363=CARTESIAN_POINT ( 'NONE',  ( -0.5999999999999999778, -5.000000000000000000, -0.5999999999999999778 ) ) ;
#41576=FACE_OUTER_BOUND ( 'NONE', #283, .T. ) ;
#41882=SURFACE_STYLE_FILL_AREA ( #55168 ) ;
#41893=CARTESIAN_POINT ( 'NONE',  ( 0.5999999999999999778, -5.000000000000000000, 0.5999999999999999778 ) ) ;
#41994=CARTESIAN_POINT ( 'NONE',  ( 4.000000000000000000, -5.200000000000000178, -0.5999999999999999778 ) ) ;
#42067=DIRECTION ( 'NONE',  ( 0.000000000000000000, -1.000000000000000000, 0.000000000000000000 ) ) ;
#42152=VECTOR ( 'NONE', #13064, 1000.000000000000000 ) ;
#42169=VERTEX_POINT ( 'NONE', #27448 ) ;
#42252=DIRECTION ( 'NONE',  ( 0.000000000000000000, -1.000000000000000000, 0.000000000000000000 ) ) ;
#42299=ORIENTED_EDGE ( 'NONE', *, *, #4441, .F. ) ;
#42416=DIRECTION ( 'NONE',  ( 0.000000000000000000, 0.000000000000000000, 1.000000000000000000 ) ) ;
#42437=EDGE_CURVE ( 'NONE', #27162, #29661, #5599, .T. ) ;
#42467=ORIENTED_EDGE ( 'NONE', *, *, #42437, .T. ) ;
#42544=ORIENTED_EDGE ( 'NONE', *, *, #21338, .T. ) ;
#42751=ORIENTED_EDGE ( 'NONE', *, *, #29293, .F. ) ;
#42756=ORIENTED_EDGE ( 'NONE', *, *, #41284, .T. ) ;
#42763=VECTOR ( 'NONE', #27669, 1000.000000000000000 ) ;
#43056=EDGE_CURVE ( 'NONE', #2598, #39462, #56820, .T. ) ;
#43079=VECTOR ( 'NONE', #9193, 1000.000000000000000 ) ;
#43120=EDGE_LOOP ( 'NONE', ( #52457, #6737, #18939, #16335 ) ) ;
#43298=FILL_AREA_STYLE_COLOUR ( '', #11341 ) ;
#43517=DIRECTION ( 'NONE',  ( 0.000000000000000000, 0.000000000000000000, 1.000000000000000000 ) ) ;
#43523=LINE ( 'NONE', #47687, #17342 ) ;
#43526=AXIS2_PLACEMENT_3D ( 'NONE', #45889, #10156, #14564 ) ;
#43552=LINE ( 'NONE', #11397, #45710 ) ;
#43570=CARTESIAN_POINT ( 'NONE',  ( 10.50000000000000000, -73.00000000000001421, 0.000000000000000000 ) ) ;
#43676=DIRECTION ( 'NONE',  ( 0.000000000000000000, 1.000000000000000000, 0.000000000000000000 ) ) ;
#43768=LINE ( 'NONE', #38454, #44416 ) ;
#43811=LINE ( 'NONE', #3357, #42152 ) ;
#43820=CARTESIAN_POINT ( 'NONE',  ( -4.000000000000000000, -5.000000000000000000, -0.5999999999999999778 ) ) ;
#43896=EDGE_CURVE ( 'NONE', #31619, #25098, #33330, .T. ) ;
#43967=CARTESIAN_POINT ( 'NONE',  ( 0.000000000000000000, -7.000000000000000000, 0.000000000000000000 ) ) ;
#43974=CARTESIAN_POINT ( 'NONE',  ( 4.000000000000000000, -5.000000000000000000, 0.5999999999999999778 ) ) ;
#44151=FACE_OUTER_BOUND ( 'NONE', #57763, .T. ) ;
#44221=DIRECTION ( 'NONE',  ( 0.000000000000000000, 1.000000000000000000, 0.000000000000000000 ) ) ;
#44329=VECTOR ( 'NONE', #26977, 1000.000000000000000 ) ;
#44378=ORIENTED_EDGE ( 'NONE', *, *, #18570, .F. ) ;
#44416=VECTOR ( 'NONE', #52051, 1000.000000000000000 ) ;
#44423=ORIENTED_EDGE ( 'NONE', *, *, #57675, .F. ) ;
#44437=ADVANCED_FACE ( 'NONE', ( #31246 ), #31545, .F. ) ;
#44482=EDGE_LOOP ( 'NONE', ( #49059, #31468, #11123, #4204, #2948, #29950, #47213, #33860, #36065, #3962, #12612, #5715 ) ) ;
#44544=ORIENTED_EDGE ( 'NONE', *, *, #14587, .F. ) ;
#44558=DIRECTION ( 'NONE',  ( 0.000000000000000000, 1.000000000000000000, 0.000000000000000000 ) ) ;
#44580=CARTESIAN_POINT ( 'NONE',  ( -4.000000000000000000, -75.00000000000001421, -0.5999999999999999778 ) ) ;
#44706=ADVANCED_FACE ( 'NONE', ( #14990 ), #51034, .F. ) ;
#44778=DIRECTION ( 'NONE',  ( 0.9998748951565024079, 0.000000000000000000, 0.01581752306063006000 ) ) ;
#45013=( NAMED_UNIT ( * ) SI_UNIT ( $, .STERADIAN. ) SOLID_ANGLE_UNIT ( ) );
#45063=AXIS2_PLACEMENT_3D ( 'NONE', #24234, #42252, #27773 ) ;
#45071=ADVANCED_FACE ( 'NONE', ( #56542 ), #49490, .T. ) ;
#45079=CARTESIAN_POINT ( 'NONE',  ( -4.000000000000000000, -75.00000000000001421, 0.5999999999999999778 ) ) ;
#45133=DIRECTION ( 'NONE',  ( 0.000000000000000000, 0.000000000000000000, -1.000000000000000000 ) ) ;
#45205=LINE ( 'NONE', #31887, #55294 ) ;
#45310=LINE ( 'NONE', #31695, #44329 ) ;
#45375=LINE ( 'NONE', #45079, #47253 ) ;
#45394=DIRECTION ( 'NONE',  ( 1.000000000000000000, 0.000000000000000000, 0.000000000000000000 ) ) ;
#45403=VECTOR ( 'NONE', #14074, 1000.000000000000000 ) ;
#45428=DIRECTION ( 'NONE',  ( 0.000000000000000000, -1.000000000000000000, 0.000000000000000000 ) ) ;
#45504=VERTEX_POINT ( 'NONE', #37875 ) ;
#45581=CARTESIAN_POINT ( 'NONE',  ( -0.5999999999999999778, -5.000000000000000000, 4.000000000000000000 ) ) ;
#45636=PLANE ( 'NONE',  #14739 ) ;
#45710=VECTOR ( 'NONE', #8110, 1000.000000000000000 ) ;
#45735=CARTESIAN_POINT ( 'NONE',  ( -0.5999999999999999778, -5.000000000000000000, 0.5999999999999999778 ) ) ;
#45752=ORIENTED_EDGE ( 'NONE', *, *, #43896, .F. ) ;
#45779=ORIENTED_EDGE ( 'NONE', *, *, #35877, .F. ) ;
#45812=EDGE_CURVE ( 'NONE', #39893, #29440, #43552, .T. ) ;
#45889=CARTESIAN_POINT ( 'NONE',  ( 0.000000000000000000, 0.000000000000000000, 0.000000000000000000 ) ) ;
#45954=CIRCLE ( 'NONE', #51598, 8.500000000000000000 ) ;
#46006=CIRCLE ( 'NONE', #3536, 8.500000000000000000 ) ;
#46029=PLANE ( 'NONE',  #5038 ) ;
#46196=DIRECTION ( 'NONE',  ( 0.000000000000000000, -1.000000000000000000, 0.000000000000000000 ) ) ;
#46197=PRODUCT_CONTEXT ( 'NONE', #58302, 'mechanical' ) ;
#46243=CARTESIAN_POINT ( 'NONE',  ( 0.5999999999999999778, -5.000000000000000000, 0.5999999999999999778 ) ) ;
#46323=VERTEX_POINT ( 'NONE', #56227 ) ;
#46405=STYLED_ITEM ( 'NONE', ( #29953 ), #35529 ) ;
#46484=ORIENTED_EDGE ( 'NONE', *, *, #4722, .F. ) ;
#46485=VERTEX_POINT ( 'NONE', #17806 ) ;
#46585=SURFACE_STYLE_USAGE ( .BOTH. , #28537 ) ;
#46882=CARTESIAN_POINT ( 'NONE',  ( -4.000000000000000000, -5.000000000000000000, -0.5999999999999999778 ) ) ;
#46924=EDGE_CURVE ( 'NONE', #34639, #22699, #36032, .T. ) ;
#46971=EDGE_CURVE ( 'NONE', #33522, #21810, #34162, .T. ) ;
#47071=DIRECTION ( 'NONE',  ( 0.000000000000000000, 0.000000000000000000, 1.000000000000000000 ) ) ;
#47072=VECTOR ( 'NONE', #25478, 1000.000000000000000 ) ;
#47213=ORIENTED_EDGE ( 'NONE', *, *, #21420, .T. ) ;
#47253=VECTOR ( 'NONE', #807, 1000.000000000000000 ) ;
#47374=PLANE ( 'NONE',  #8677 ) ;
#47471=PLANE ( 'NONE',  #105 ) ;
#47656=EDGE_CURVE ( 'NONE', #29440, #46485, #15980, .T. ) ;
#47687=CARTESIAN_POINT ( 'NONE',  ( 0.5999999999999999778, -5.000000000000000000, -4.000000000000000000 ) ) ;
#47723=ORIENTED_EDGE ( 'NONE', *, *, #33846, .F. ) ;
#47845=FACE_OUTER_BOUND ( 'NONE', #14704, .T. ) ;
#47931=EDGE_CURVE ( 'NONE', #52567, #2048, #18657, .T. ) ;
#48050=CARTESIAN_POINT ( 'NONE',  ( 4.000000000000000000, -74.80000000000001137, 0.5999999999999999778 ) ) ;
#48248=DIRECTION ( 'NONE',  ( -1.000000000000000000, 0.000000000000000000, 0.000000000000000000 ) ) ;
#48404=DIRECTION ( 'NONE',  ( 0.000000000000000000, 1.000000000000000000, 0.000000000000000000 ) ) ;
#48736=ORIENTED_EDGE ( 'NONE', *, *, #53504, .F. ) ;
#48764=VECTOR ( 'NONE', #127, 1000.000000000000000 ) ;
#48855=DIRECTION ( 'NONE',  ( 1.000000000000000000, 0.000000000000000000, 0.000000000000000000 ) ) ;
#48938=LINE ( 'NONE', #26199, #54632 ) ;
#49059=ORIENTED_EDGE ( 'NONE', *, *, #25817, .T. ) ;
#49063=DIRECTION ( 'NONE',  ( 0.000000000000000000, -1.000000000000000000, 0.000000000000000000 ) ) ;
#49065=ORIENTED_EDGE ( 'NONE', *, *, #7631, .F. ) ;
#49207=( GEOMETRIC_REPRESENTATION_CONTEXT ( 3 ) GLOBAL_UNCERTAINTY_ASSIGNED_CONTEXT ( ( #20127 ) ) GLOBAL_UNIT_ASSIGNED_CONTEXT ( ( #10015, #28284, #14710 ) ) REPRESENTATION_CONTEXT ( 'NONE', 'WORKASPACE' ) );
#49259=DIRECTION ( 'NONE',  ( 1.000000000000000000, 0.000000000000000000, 0.000000000000000000 ) ) ;
#49377=EDGE_LOOP ( 'NONE', ( #58357, #20255, #24887, #12602 ) ) ;
#49404=CARTESIAN_POINT ( 'NONE',  ( -4.000000000000000000, -75.00000000000001421, -0.5999999999999999778 ) ) ;
#49469=LINE ( 'NONE', #22879, #31235 ) ;
#49474=CARTESIAN_POINT ( 'NONE',  ( 4.000000000000000000, -75.00000000000001421, -0.5999999999999999778 ) ) ;
#49490=TOROIDAL_SURFACE ( 'NONE', #34378, 8.500000000000000000, 2.000000000000000000 ) ;
#49524=VECTOR ( 'NONE', #30637, 1000.000000000000000 ) ;
#49695=CARTESIAN_POINT ( 'NONE',  ( 10.50000000000000000, -7.000000000000000000, 5.990617821004000856E-12 ) ) ;
#49746=CARTESIAN_POINT ( 'NONE',  ( -4.000000000000000000, -5.200000000000000178, -0.5999999999999999778 ) ) ;
#49867=DIRECTION ( 'NONE',  ( 0.000000000000000000, -1.000000000000000000, 0.000000000000000000 ) ) ;
#50008=VECTOR ( 'NONE', #16761, 1000.000000000000000 ) ;
#50032=FACE_OUTER_BOUND ( 'NONE', #33707, .T. ) ;
#50057=CARTESIAN_POINT ( 'NONE',  ( -4.000000000000000000, -74.80000000000001137, -0.5999999999999999778 ) ) ;
#50112=LINE ( 'NONE', #22648, #31161 ) ;
#50181=DIRECTION ( 'NONE',  ( 0.000000000000000000, 0.000000000000000000, 1.000000000000000000 ) ) ;
#50191=DIRECTION ( 'NONE',  ( 0.000000000000000000, -1.000000000000000000, 0.000000000000000000 ) ) ;
#50295=EDGE_CURVE ( 'NONE', #45504, #52567, #50112, .T. ) ;
#50323=FACE_OUTER_BOUND ( 'NONE', #16410, .T. ) ;
#50349=VECTOR ( 'NONE', #19195, 1000.000000000000000 ) ;
#50470=EDGE_CURVE ( 'NONE', #53803, #46485, #37967, .T. ) ;
#50484=DIRECTION ( 'NONE',  ( 0.000000000000000000, 0.000000000000000000, -1.000000000000000000 ) ) ;
#50507=DIRECTION ( 'NONE',  ( 0.000000000000000000, -1.000000000000000000, 0.000000000000000000 ) ) ;
#50530=ORIENTED_EDGE ( 'NONE', *, *, #6764, .F. ) ;
#50637=VECTOR ( 'NONE', #57586, 1000.000000000000000 ) ;
#50681=VECTOR ( 'NONE', #36732, 1000.000000000000000 ) ;
#50778=DIRECTION ( 'NONE',  ( 1.000000000000000000, 0.000000000000000000, 0.000000000000000000 ) ) ;
#50822=LINE ( 'NONE', #9786, #34667 ) ;
#50873=( GEOMETRIC_REPRESENTATION_CONTEXT ( 3 ) GLOBAL_UNCERTAINTY_ASSIGNED_CONTEXT ( ( #13262 ) ) GLOBAL_UNIT_ASSIGNED_CONTEXT ( ( #3121, #3403, #45013 ) ) REPRESENTATION_CONTEXT ( 'NONE', 'WORKASPACE' ) );
#50895=ORIENTED_EDGE ( 'NONE', *, *, #36182, .F. ) ;
#50932=AXIS2_PLACEMENT_3D ( 'NONE', #51201, #47071, #6307 ) ;
#50966=ORIENTED_EDGE ( 'NONE', *, *, #40673, .F. ) ;
#50973=TOROIDAL_SURFACE ( 'NONE', #25495, 8.500000000000000000, 2.000000000000000000 ) ;
#50998=EDGE_CURVE ( 'NONE', #55898, #13579, #43768, .T. ) ;
#51012=FACE_OUTER_BOUND ( 'NONE', #55688, .T. ) ;
#51034=PLANE ( 'NONE',  #24916 ) ;
#51110=LINE ( 'NONE', #10664, #11026 ) ;
#51201=CARTESIAN_POINT ( 'NONE',  ( 4.000000000000000000, -75.00000000000001421, 0.5999999999999999778 ) ) ;
#51305=DIRECTION ( 'NONE',  ( -1.000000000000000000, 0.000000000000000000, 0.000000000000000000 ) ) ;
#51499=EDGE_LOOP ( 'NONE', ( #53730, #25599, #52653, #28254 ) ) ;
#51500=ORIENTED_EDGE ( 'NONE', *, *, #45812, .F. ) ;
#51552=CARTESIAN_POINT ( 'NONE',  ( -0.5999999999999999778, -5.200000000000000178, 4.000000000000000000 ) ) ;
#51598=AXIS2_PLACEMENT_3D ( 'NONE', #10547, #23816, #24113 ) ;
#51686=VERTEX_POINT ( 'NONE', #5210 ) ;
#51722=AXIS2_PLACEMENT_3D ( 'NONE', #433, #31961, #13078 ) ;
#51759=ADVANCED_FACE ( 'NONE', ( #54225 ), #19018, .T. ) ;
#51841=DIRECTION ( 'NONE',  ( 0.000000000000000000, -1.000000000000000000, 0.000000000000000000 ) ) ;
#51849=EDGE_CURVE ( 'NONE', #22214, #36179, #55971, .T. ) ;
#51875=( NAMED_UNIT ( * ) PLANE_ANGLE_UNIT ( ) SI_UNIT ( $, .RADIAN. ) );
#51881=MECHANICAL_DESIGN_GEOMETRIC_PRESENTATION_REPRESENTATION('',(#36766),#39628);
#51903=VERTEX_POINT ( 'NONE', #28200 ) ;
#51904=EDGE_CURVE ( 'NONE', #670, #35536, #15523, .T. ) ;
#52051=DIRECTION ( 'NONE',  ( 0.000000000000000000, -1.000000000000000000, 0.000000000000000000 ) ) ;
#52117=CARTESIAN_POINT ( 'NONE',  ( 0.5999999999999999778, -5.000000000000000000, 4.000000000000000000 ) ) ;
#52350=ORIENTED_EDGE ( 'NONE', *, *, #23570, .F. ) ;
#52373=CARTESIAN_POINT ( 'NONE',  ( -4.000000000000000000, -75.00000000000001421, 0.5999999999999999778 ) ) ;
#52388=VECTOR ( 'NONE', #7924, 1000.000000000000000 ) ;
#52457=ORIENTED_EDGE ( 'NONE', *, *, #14587, .T. ) ;
#52567=VERTEX_POINT ( 'NONE', #69 ) ;
#52639=EDGE_CURVE ( 'NONE', #20634, #670, #22463, .T. ) ;
#52653=ORIENTED_EDGE ( 'NONE', *, *, #51849, .F. ) ;
#52702=FACE_OUTER_BOUND ( 'NONE', #23287, .T. ) ;
#52703=SURFACE_STYLE_USAGE ( .BOTH. , #57700 ) ;
#52950=DIRECTION ( 'NONE',  ( 0.000000000000000000, 1.000000000000000000, 0.000000000000000000 ) ) ;
#52976=CARTESIAN_POINT ( 'NONE',  ( 10.50000000000000000, -7.000000000000000000, 0.000000000000000000 ) ) ;
#53036=EDGE_CURVE ( 'NONE', #22633, #2598, #15872, .T. ) ;
#53361=CARTESIAN_POINT ( 'NONE',  ( 0.000000000000000000, -5.000000000000000000, 0.000000000000000000 ) ) ;
#53419=CARTESIAN_POINT ( 'NONE',  ( -8.500000000000000000, -5.000000000000000000, 0.000000000000000000 ) ) ;
#53504=EDGE_CURVE ( 'NONE', #11048, #45504, #54817, .T. ) ;
#53730=ORIENTED_EDGE ( 'NONE', *, *, #50998, .T. ) ;
#53768=DIRECTION ( 'NONE',  ( 0.000000000000000000, -1.000000000000000000, 0.000000000000000000 ) ) ;
#53803=VERTEX_POINT ( 'NONE', #54674 ) ;
#53806=ADVANCED_FACE ( 'NONE', ( #41093 ), #969, .T. ) ;
#53824=LINE ( 'NONE', #49695, #48764 ) ;
#53902=DIRECTION ( 'NONE',  ( 1.000000000000000000, 0.000000000000000000, -0.000000000000000000 ) ) ;
#54095=ORIENTED_EDGE ( 'NONE', *, *, #25472, .F. ) ;
#54123=ORIENTED_EDGE ( 'NONE', *, *, #25472, .T. ) ;
#54160=PLANE ( 'NONE',  #24533 ) ;
#54176=VECTOR ( 'NONE', #21400, 1000.000000000000000 ) ;
#54225=FACE_OUTER_BOUND ( 'NONE', #19519, .T. ) ;
#54562=DIRECTION ( 'NONE',  ( 0.000000000000000000, -1.000000000000000000, 0.000000000000000000 ) ) ;
#54632=VECTOR ( 'NONE', #8481, 1000.000000000000000 ) ;
#54674=CARTESIAN_POINT ( 'NONE',  ( -0.5999999999999999778, -5.200000000000000178, -4.000000000000000000 ) ) ;
#54684=EDGE_CURVE ( 'NONE', #35302, #11183, #49469, .T. ) ;
#54782=CARTESIAN_POINT ( 'NONE',  ( 0.5999999999999999778, -5.000000000000000000, -0.5999999999999999778 ) ) ;
#54817=LINE ( 'NONE', #26763, #45403 ) ;
#54894=CARTESIAN_POINT ( 'NONE',  ( 4.000000000000000000, -5.200000000000000178, 0.5999999999999999778 ) ) ;
#55099=EDGE_CURVE ( 'NONE', #35536, #57897, #14197, .T. ) ;
#55168=FILL_AREA_STYLE ('',( #19160 ) ) ;
#55210=LINE ( 'NONE', #15356, #23902 ) ;
#55294=VECTOR ( 'NONE', #53768, 1000.000000000000000 ) ;
#55363=LINE ( 'NONE', #54782, #11797 ) ;
#55507=EDGE_CURVE ( 'NONE', #22633, #35536, #45310, .T. ) ;
#55528=DIRECTION ( 'NONE',  ( -1.000000000000000000, 0.000000000000000000, 0.000000000000000000 ) ) ;
#55688=EDGE_LOOP ( 'NONE', ( #91, #40568, #30462, #54123 ) ) ;
#55725=DIRECTION ( 'NONE',  ( 0.000000000000000000, -1.000000000000000000, 0.000000000000000000 ) ) ;
#55742=CARTESIAN_POINT ( 'NONE',  ( 0.5999999999999999778, -5.000000000000000000, 4.000000000000000000 ) ) ;
#55743=FACE_OUTER_BOUND ( 'NONE', #5976, .T. ) ;
#55898=VERTEX_POINT ( 'NONE', #3484 ) ;
#55971=LINE ( 'NONE', #29090, #1124 ) ;
#55988=EDGE_LOOP ( 'NONE', ( #25753, #12884, #42756, #42467 ) ) ;
#56073=EDGE_CURVE ( 'NONE', #34639, #31619, #14136, .T. ) ;
#56094=ADVANCED_FACE ( 'NONE', ( #14666 ), #5817, .F. ) ;
#56118=ORIENTED_EDGE ( 'NONE', *, *, #167, .F. ) ;
#56140=DIRECTION ( 'NONE',  ( 0.000000000000000000, -1.000000000000000000, 0.000000000000000000 ) ) ;
#56227=CARTESIAN_POINT ( 'NONE',  ( -8.500000000000000000, -75.00000000000001421, 0.000000000000000000 ) ) ;
#56346=MANIFOLD_SOLID_BREP ( 'Stock-MAS-694-1', #2267 ) ;
#56390=ORIENTED_EDGE ( 'NONE', *, *, #17914, .T. ) ;
#56542=FACE_OUTER_BOUND ( 'NONE', #49377, .T. ) ;
#56570=ADVANCED_FACE ( 'NONE', ( #24717 ), #47471, .F. ) ;
#56620=ORIENTED_EDGE ( 'NONE', *, *, #25748, .F. ) ;
#56687=CARTESIAN_POINT ( 'NONE',  ( 0.5999999999999999778, -5.000000000000000000, -4.000000000000000000 ) ) ;
#56759=COLOUR_RGB ( '', 0.09019608, 0.27058824, 0.51372549) ;
#56806=CARTESIAN_POINT ( 'NONE',  ( -4.000000000000000000, -5.200000000000000178, -0.5999999999999999778 ) ) ;
#56820=LINE ( 'NONE', #34359, #13451 ) ;
#56970=DIRECTION ( 'NONE',  ( 0.000000000000000000, 1.000000000000000000, 0.000000000000000000 ) ) ;
#57000=CARTESIAN_POINT ( 'NONE',  ( 4.000000000000000000, -5.000000000000000000, -0.5999999999999999778 ) ) ;
#57073=DIRECTION ( 'NONE',  ( 0.000000000000000000, 0.000000000000000000, -1.000000000000000000 ) ) ;
#57362=DIRECTION ( 'NONE',  ( 0.000000000000000000, 1.000000000000000000, 0.000000000000000000 ) ) ;
#57586=DIRECTION ( 'NONE',  ( 1.000000000000000000, 0.000000000000000000, 0.000000000000000000 ) ) ;
#57675=EDGE_CURVE ( 'NONE', #34134, #27162, #45375, .T. ) ;
#57698=ORIENTED_EDGE ( 'NONE', *, *, #43056, .F. ) ;
#57700=SURFACE_SIDE_STYLE ('',( #41882 ) ) ;
#57713=DIRECTION ( 'NONE',  ( -1.000000000000000000, 0.000000000000000000, 0.000000000000000000 ) ) ;
#57739=CARTESIAN_POINT ( 'NONE',  ( 0.5999999999999999778, -5.000000000000000000, -4.000000000000000000 ) ) ;
#57763=EDGE_LOOP ( 'NONE', ( #24617, #24607, #44423, #4644 ) ) ;
#57875=CARTESIAN_POINT ( 'NONE',  ( 4.000000000000000000, -75.00000000000001421, -0.5999999999999999778 ) ) ;
#57897=VERTEX_POINT ( 'NONE', #29089 ) ;
#57957=EDGE_LOOP ( 'NONE', ( #23278, #51500, #42299, #36859, #10090, #50966, #57698, #12103, #54095, #22923, #22411, #48736 ) ) ;
#57961=CARTESIAN_POINT ( 'NONE',  ( 8.500000000000000000, -5.000000000000000000, 0.000000000000000000 ) ) ;
#58176=DIRECTION ( 'NONE',  ( 0.000000000000000000, -1.000000000000000000, 0.000000000000000000 ) ) ;
#58302=APPLICATION_CONTEXT ( 'automotive_design' ) ;
#58357=ORIENTED_EDGE ( 'NONE', *, *, #23570, .T. ) ;
ENDSEC;
END-ISO-10303-21;
